ISO-10303-21;
HEADER;
/* Generated by software containing ST-Developer
 * from STEP Tools, Inc. (www.steptools.com) 
 */

FILE_DESCRIPTION(
/* description */ ('Lever-operated bar clamp (toggle)'),
/* implementation_level */ '2;1');

FILE_NAME(
/* name */ 'M4x10 Cap Screw.step',
/* time_stamp */ '2026-10-28T03:25:02-07:00',
/* author */ (''),
/* organization */ (''),
/* preprocessor_version */ 'ST-DEVELOPER v20.2',
/* originating_system */ 'Autodesk Translation Framework v15.17.0.0',
/* authorisation */ '');

FILE_SCHEMA (('AUTOMOTIVE_DESIGN { 1 0 10303 214 3 1 1 }'));
ENDSEC;

DATA;
#10=MECHANICAL_DESIGN_GEOMETRIC_PRESENTATION_REPRESENTATION('',(#447),#12413);
#317=CONICAL_SURFACE('',#7691,0.325,0.785398163397448);
#318=CONICAL_SURFACE('',#7695,0.335,0.785398163397448);
#319=CONICAL_SURFACE('',#7699,0.21,0.463647609000806);
#328=ORIENTED_CLOSED_SHELL('',*,#6608,.F.);
#332=BREP_WITH_VOIDS('Body1',#6609,(#328));
#363=SHAPE_REPRESENTATION_RELATIONSHIP('SRR','None',#12605,#401);
#401=ADVANCED_BREP_SHAPE_REPRESENTATION('',(#332),#12402);
#447=STYLED_ITEM('',(#12876),#332);
#634=FACE_BOUND('',#1755,.T.);
#825=PLANE('',#7679);
#826=PLANE('',#7680);
#827=PLANE('',#7681);
#828=PLANE('',#7682);
#829=PLANE('',#7683);
#830=PLANE('',#7684);
#831=PLANE('',#7685);
#832=PLANE('',#7686);
#833=PLANE('',#7687);
#834=PLANE('',#7689);
#835=PLANE('',#7697);
#1201=FACE_OUTER_BOUND('',#1741,.T.);
#1202=FACE_OUTER_BOUND('',#1742,.T.);
#1203=FACE_OUTER_BOUND('',#1743,.T.);
#1204=FACE_OUTER_BOUND('',#1744,.T.);
#1205=FACE_OUTER_BOUND('',#1745,.T.);
#1206=FACE_OUTER_BOUND('',#1746,.T.);
#1207=FACE_OUTER_BOUND('',#1747,.T.);
#1208=FACE_OUTER_BOUND('',#1748,.T.);
#1209=FACE_OUTER_BOUND('',#1749,.T.);
#1210=FACE_OUTER_BOUND('',#1750,.T.);
#1211=FACE_OUTER_BOUND('',#1751,.T.);
#1212=FACE_OUTER_BOUND('',#1752,.T.);
#1213=FACE_OUTER_BOUND('',#1753,.T.);
#1214=FACE_OUTER_BOUND('',#1754,.T.);
#1215=FACE_OUTER_BOUND('',#1756,.T.);
#1216=FACE_OUTER_BOUND('',#1757,.T.);
#1741=EDGE_LOOP('',(#5669,#5670,#5671,#5672));
#1742=EDGE_LOOP('',(#5673,#5674,#5675,#5676));
#1743=EDGE_LOOP('',(#5677,#5678,#5679,#5680));
#1744=EDGE_LOOP('',(#5681,#5682,#5683,#5684));
#1745=EDGE_LOOP('',(#5685,#5686,#5687,#5688));
#1746=EDGE_LOOP('',(#5689,#5690,#5691,#5692));
#1747=EDGE_LOOP('',(#5693,#5694,#5695,#5696,#5697,#5698));
#1748=EDGE_LOOP('',(#5699,#5700,#5701,#5702,#5703,#5704));
#1749=EDGE_LOOP('',(#5705));
#1750=EDGE_LOOP('',(#5706));
#1751=EDGE_LOOP('',(#5707,#5708,#5709,#5710));
#1752=EDGE_LOOP('',(#5711,#5712,#5713,#5714));
#1753=EDGE_LOOP('',(#5715,#5716,#5717,#5718));
#1754=EDGE_LOOP('',(#5719));
#1755=EDGE_LOOP('',(#5720));
#1756=EDGE_LOOP('',(#5721,#5722,#5723,#5724));
#1757=EDGE_LOOP('',(#5725,#5726,#5727,#5728));
#2168=LINE('',#11848,#2609);
#2169=LINE('',#11850,#2610);
#2170=LINE('',#11852,#2611);
#2171=LINE('',#11853,#2612);
#2172=LINE('',#11856,#2613);
#2173=LINE('',#11858,#2614);
#2174=LINE('',#11859,#2615);
#2175=LINE('',#11862,#2616);
#2176=LINE('',#11864,#2617);
#2177=LINE('',#11865,#2618);
#2178=LINE('',#11868,#2619);
#2179=LINE('',#11870,#2620);
#2180=LINE('',#11871,#2621);
#2181=LINE('',#11874,#2622);
#2182=LINE('',#11876,#2623);
#2183=LINE('',#11877,#2624);
#2184=LINE('',#11879,#2625);
#2185=LINE('',#11880,#2626);
#2186=LINE('',#11892,#2627);
#2187=LINE('',#11896,#2628);
#2188=LINE('',#11900,#2629);
#2189=LINE('',#11907,#2630);
#2190=LINE('',#11909,#2631);
#2609=VECTOR('',#9493,1.);
#2610=VECTOR('',#9494,1.);
#2611=VECTOR('',#9495,1.);
#2612=VECTOR('',#9496,1.);
#2613=VECTOR('',#9499,1.);
#2614=VECTOR('',#9500,1.);
#2615=VECTOR('',#9501,1.);
#2616=VECTOR('',#9504,1.);
#2617=VECTOR('',#9505,1.);
#2618=VECTOR('',#9506,1.);
#2619=VECTOR('',#9509,1.);
#2620=VECTOR('',#9510,1.);
#2621=VECTOR('',#9511,1.);
#2622=VECTOR('',#9514,1.);
#2623=VECTOR('',#9515,1.);
#2624=VECTOR('',#9516,1.);
#2625=VECTOR('',#9519,1.);
#2626=VECTOR('',#9520,1.);
#2627=VECTOR('',#9537,0.325);
#2628=VECTOR('',#9542,0.35);
#2629=VECTOR('',#9547,0.335);
#2630=VECTOR('',#9556,0.21);
#2631=VECTOR('',#9559,0.2);
#3018=CIRCLE('',#7688,0.1954);
#3019=CIRCLE('',#7690,0.3);
#3020=CIRCLE('',#7692,0.35);
#3021=CIRCLE('',#7694,0.35);
#3022=CIRCLE('',#7696,0.32);
#3023=CIRCLE('',#7698,0.22);
#3024=CIRCLE('',#7700,0.1954);
#3497=VERTEX_POINT('',#11846);
#3498=VERTEX_POINT('',#11847);
#3499=VERTEX_POINT('',#11849);
#3500=VERTEX_POINT('',#11851);
#3501=VERTEX_POINT('',#11855);
#3502=VERTEX_POINT('',#11857);
#3503=VERTEX_POINT('',#11861);
#3504=VERTEX_POINT('',#11863);
#3505=VERTEX_POINT('',#11867);
#3506=VERTEX_POINT('',#11869);
#3507=VERTEX_POINT('',#11873);
#3508=VERTEX_POINT('',#11875);
#3509=VERTEX_POINT('',#11884);
#3510=VERTEX_POINT('',#11887);
#3511=VERTEX_POINT('',#11890);
#3512=VERTEX_POINT('',#11894);
#3513=VERTEX_POINT('',#11898);
#3514=VERTEX_POINT('',#11902);
#3515=VERTEX_POINT('',#11905);
#4239=EDGE_CURVE('',#3497,#3498,#2168,.T.);
#4240=EDGE_CURVE('',#3498,#3499,#2169,.T.);
#4241=EDGE_CURVE('',#3499,#3500,#2170,.T.);
#4242=EDGE_CURVE('',#3497,#3500,#2171,.T.);
#4243=EDGE_CURVE('',#3498,#3501,#2172,.T.);
#4244=EDGE_CURVE('',#3501,#3502,#2173,.T.);
#4245=EDGE_CURVE('',#3502,#3499,#2174,.T.);
#4246=EDGE_CURVE('',#3501,#3503,#2175,.T.);
#4247=EDGE_CURVE('',#3503,#3504,#2176,.T.);
#4248=EDGE_CURVE('',#3504,#3502,#2177,.T.);
#4249=EDGE_CURVE('',#3503,#3505,#2178,.T.);
#4250=EDGE_CURVE('',#3505,#3506,#2179,.T.);
#4251=EDGE_CURVE('',#3506,#3504,#2180,.T.);
#4252=EDGE_CURVE('',#3505,#3507,#2181,.T.);
#4253=EDGE_CURVE('',#3507,#3508,#2182,.T.);
#4254=EDGE_CURVE('',#3508,#3506,#2183,.T.);
#4255=EDGE_CURVE('',#3507,#3497,#2184,.T.);
#4256=EDGE_CURVE('',#3500,#3508,#2185,.T.);
#4257=EDGE_CURVE('',#3509,#3509,#3018,.T.);
#4258=EDGE_CURVE('',#3510,#3510,#3019,.T.);
#4259=EDGE_CURVE('',#3511,#3511,#3020,.T.);
#4260=EDGE_CURVE('',#3511,#3510,#2186,.T.);
#4261=EDGE_CURVE('',#3512,#3512,#3021,.T.);
#4262=EDGE_CURVE('',#3512,#3511,#2187,.T.);
#4263=EDGE_CURVE('',#3513,#3513,#3022,.T.);
#4264=EDGE_CURVE('',#3513,#3512,#2188,.T.);
#4265=EDGE_CURVE('',#3514,#3514,#3023,.T.);
#4266=EDGE_CURVE('',#3515,#3515,#3024,.F.);
#4267=EDGE_CURVE('',#3515,#3514,#2189,.T.);
#4268=EDGE_CURVE('',#3509,#3515,#2190,.T.);
#5669=ORIENTED_EDGE('',*,*,#4239,.T.);
#5670=ORIENTED_EDGE('',*,*,#4240,.T.);
#5671=ORIENTED_EDGE('',*,*,#4241,.T.);
#5672=ORIENTED_EDGE('',*,*,#4242,.F.);
#5673=ORIENTED_EDGE('',*,*,#4243,.T.);
#5674=ORIENTED_EDGE('',*,*,#4244,.T.);
#5675=ORIENTED_EDGE('',*,*,#4245,.T.);
#5676=ORIENTED_EDGE('',*,*,#4240,.F.);
#5677=ORIENTED_EDGE('',*,*,#4246,.T.);
#5678=ORIENTED_EDGE('',*,*,#4247,.T.);
#5679=ORIENTED_EDGE('',*,*,#4248,.T.);
#5680=ORIENTED_EDGE('',*,*,#4244,.F.);
#5681=ORIENTED_EDGE('',*,*,#4249,.T.);
#5682=ORIENTED_EDGE('',*,*,#4250,.T.);
#5683=ORIENTED_EDGE('',*,*,#4251,.T.);
#5684=ORIENTED_EDGE('',*,*,#4247,.F.);
#5685=ORIENTED_EDGE('',*,*,#4252,.T.);
#5686=ORIENTED_EDGE('',*,*,#4253,.T.);
#5687=ORIENTED_EDGE('',*,*,#4254,.T.);
#5688=ORIENTED_EDGE('',*,*,#4250,.F.);
#5689=ORIENTED_EDGE('',*,*,#4255,.T.);
#5690=ORIENTED_EDGE('',*,*,#4242,.T.);
#5691=ORIENTED_EDGE('',*,*,#4256,.T.);
#5692=ORIENTED_EDGE('',*,*,#4253,.F.);
#5693=ORIENTED_EDGE('',*,*,#4255,.F.);
#5694=ORIENTED_EDGE('',*,*,#4252,.F.);
#5695=ORIENTED_EDGE('',*,*,#4249,.F.);
#5696=ORIENTED_EDGE('',*,*,#4246,.F.);
#5697=ORIENTED_EDGE('',*,*,#4243,.F.);
#5698=ORIENTED_EDGE('',*,*,#4239,.F.);
#5699=ORIENTED_EDGE('',*,*,#4256,.F.);
#5700=ORIENTED_EDGE('',*,*,#4241,.F.);
#5701=ORIENTED_EDGE('',*,*,#4245,.F.);
#5702=ORIENTED_EDGE('',*,*,#4248,.F.);
#5703=ORIENTED_EDGE('',*,*,#4251,.F.);
#5704=ORIENTED_EDGE('',*,*,#4254,.F.);
#5705=ORIENTED_EDGE('',*,*,#4257,.F.);
#5706=ORIENTED_EDGE('',*,*,#4258,.F.);
#5707=ORIENTED_EDGE('',*,*,#4259,.F.);
#5708=ORIENTED_EDGE('',*,*,#4260,.T.);
#5709=ORIENTED_EDGE('',*,*,#4258,.T.);
#5710=ORIENTED_EDGE('',*,*,#4260,.F.);
#5711=ORIENTED_EDGE('',*,*,#4261,.F.);
#5712=ORIENTED_EDGE('',*,*,#4262,.T.);
#5713=ORIENTED_EDGE('',*,*,#4259,.T.);
#5714=ORIENTED_EDGE('',*,*,#4262,.F.);
#5715=ORIENTED_EDGE('',*,*,#4263,.F.);
#5716=ORIENTED_EDGE('',*,*,#4264,.T.);
#5717=ORIENTED_EDGE('',*,*,#4261,.T.);
#5718=ORIENTED_EDGE('',*,*,#4264,.F.);
#5719=ORIENTED_EDGE('',*,*,#4263,.T.);
#5720=ORIENTED_EDGE('',*,*,#4265,.F.);
#5721=ORIENTED_EDGE('',*,*,#4266,.F.);
#5722=ORIENTED_EDGE('',*,*,#4267,.T.);
#5723=ORIENTED_EDGE('',*,*,#4265,.T.);
#5724=ORIENTED_EDGE('',*,*,#4267,.F.);
#5725=ORIENTED_EDGE('',*,*,#4257,.T.);
#5726=ORIENTED_EDGE('',*,*,#4268,.T.);
#5727=ORIENTED_EDGE('',*,*,#4266,.T.);
#5728=ORIENTED_EDGE('',*,*,#4268,.F.);
#6142=CYLINDRICAL_SURFACE('',#7693,0.35);
#6143=CYLINDRICAL_SURFACE('',#7701,0.1954);
#6476=ADVANCED_FACE('',(#1201),#825,.F.);
#6477=ADVANCED_FACE('',(#1202),#826,.F.);
#6478=ADVANCED_FACE('',(#1203),#827,.F.);
#6479=ADVANCED_FACE('',(#1204),#828,.F.);
#6480=ADVANCED_FACE('',(#1205),#829,.F.);
#6481=ADVANCED_FACE('',(#1206),#830,.F.);
#6482=ADVANCED_FACE('',(#1207),#831,.F.);
#6483=ADVANCED_FACE('',(#1208),#832,.F.);
#6484=ADVANCED_FACE('',(#1209),#833,.F.);
#6485=ADVANCED_FACE('',(#1210),#834,.T.);
#6486=ADVANCED_FACE('',(#1211),#317,.T.);
#6487=ADVANCED_FACE('',(#1212),#6142,.T.);
#6488=ADVANCED_FACE('',(#1213),#318,.T.);
#6489=ADVANCED_FACE('',(#1214,#634),#835,.T.);
#6490=ADVANCED_FACE('',(#1215),#319,.T.);
#6491=ADVANCED_FACE('',(#1216),#6143,.T.);
#6608=CLOSED_SHELL('',(#6476,#6477,#6478,#6479,#6480,#6481,#6482,#6483));
#6609=CLOSED_SHELL('',(#6484,#6485,#6486,#6487,#6488,#6489,#6490,#6491));
#7678=AXIS2_PLACEMENT_3D('',#11844,#9489,#9490);
#7679=AXIS2_PLACEMENT_3D('',#11845,#9491,#9492);
#7680=AXIS2_PLACEMENT_3D('',#11854,#9497,#9498);
#7681=AXIS2_PLACEMENT_3D('',#11860,#9502,#9503);
#7682=AXIS2_PLACEMENT_3D('',#11866,#9507,#9508);
#7683=AXIS2_PLACEMENT_3D('',#11872,#9512,#9513);
#7684=AXIS2_PLACEMENT_3D('',#11878,#9517,#9518);
#7685=AXIS2_PLACEMENT_3D('',#11881,#9521,#9522);
#7686=AXIS2_PLACEMENT_3D('',#11882,#9523,#9524);
#7687=AXIS2_PLACEMENT_3D('',#11883,#9525,#9526);
#7688=AXIS2_PLACEMENT_3D('',#11885,#9527,#9528);
#7689=AXIS2_PLACEMENT_3D('',#11886,#9529,#9530);
#7690=AXIS2_PLACEMENT_3D('',#11888,#9531,#9532);
#7691=AXIS2_PLACEMENT_3D('',#11889,#9533,#9534);
#7692=AXIS2_PLACEMENT_3D('',#11891,#9535,#9536);
#7693=AXIS2_PLACEMENT_3D('',#11893,#9538,#9539);
#7694=AXIS2_PLACEMENT_3D('',#11895,#9540,#9541);
#7695=AXIS2_PLACEMENT_3D('',#11897,#9543,#9544);
#7696=AXIS2_PLACEMENT_3D('',#11899,#9545,#9546);
#7697=AXIS2_PLACEMENT_3D('',#11901,#9548,#9549);
#7698=AXIS2_PLACEMENT_3D('',#11903,#9550,#9551);
#7699=AXIS2_PLACEMENT_3D('',#11904,#9552,#9553);
#7700=AXIS2_PLACEMENT_3D('',#11906,#9554,#9555);
#7701=AXIS2_PLACEMENT_3D('',#11908,#9557,#9558);
#9489=DIRECTION('axis',(0.,0.,1.));
#9490=DIRECTION('refdir',(1.,0.,0.));
#9491=DIRECTION('center_axis',(0.866025403784439,0.,-0.5));
#9492=DIRECTION('ref_axis',(0.5,0.,0.866025403784439));
#9493=DIRECTION('',(-0.5,0.,-0.866025403784439));
#9494=DIRECTION('',(0.,-1.,0.));
#9495=DIRECTION('',(0.5,0.,0.866025403784439));
#9496=DIRECTION('',(0.,-1.,0.));
#9497=DIRECTION('center_axis',(1.60246890531964E-16,0.,-1.));
#9498=DIRECTION('ref_axis',(1.,0.,1.60246890531964E-16));
#9499=DIRECTION('',(-1.,0.,-1.60246890531964E-16));
#9500=DIRECTION('',(0.,-1.,0.));
#9501=DIRECTION('',(1.,0.,1.60246890531964E-16));
#9502=DIRECTION('center_axis',(-0.866025403784439,0.,-0.5));
#9503=DIRECTION('ref_axis',(0.5,0.,-0.866025403784439));
#9504=DIRECTION('',(-0.5,0.,0.866025403784439));
#9505=DIRECTION('',(0.,-1.,0.));
#9506=DIRECTION('',(0.5,0.,-0.866025403784439));
#9507=DIRECTION('center_axis',(-0.866025403784439,0.,0.5));
#9508=DIRECTION('ref_axis',(-0.5,0.,-0.866025403784439));
#9509=DIRECTION('',(0.5,0.,0.866025403784439));
#9510=DIRECTION('',(0.,-1.,0.));
#9511=DIRECTION('',(-0.5,0.,-0.866025403784439));
#9512=DIRECTION('center_axis',(-1.60246890531964E-16,0.,1.));
#9513=DIRECTION('ref_axis',(-1.,0.,-1.60246890531964E-16));
#9514=DIRECTION('',(1.,0.,1.60246890531964E-16));
#9515=DIRECTION('',(0.,-1.,0.));
#9516=DIRECTION('',(-1.,0.,-1.60246890531964E-16));
#9517=DIRECTION('center_axis',(0.866025403784439,0.,0.5));
#9518=DIRECTION('ref_axis',(-0.5,0.,0.866025403784439));
#9519=DIRECTION('',(0.5,0.,-0.866025403784439));
#9520=DIRECTION('',(-0.5,0.,0.866025403784439));
#9521=DIRECTION('center_axis',(0.,1.,0.));
#9522=DIRECTION('ref_axis',(1.,0.,0.));
#9523=DIRECTION('center_axis',(0.,-1.,0.));
#9524=DIRECTION('ref_axis',(0.,0.,-1.));
#9525=DIRECTION('center_axis',(0.,1.,0.));
#9526=DIRECTION('ref_axis',(1.,0.,0.));
#9527=DIRECTION('center_axis',(0.,1.,0.));
#9528=DIRECTION('ref_axis',(1.,0.,0.));
#9529=DIRECTION('center_axis',(0.,1.,0.));
#9530=DIRECTION('ref_axis',(0.,0.,1.));
#9531=DIRECTION('center_axis',(0.,-1.,0.));
#9532=DIRECTION('ref_axis',(1.,0.,0.));
#9533=DIRECTION('center_axis',(0.,-1.,0.));
#9534=DIRECTION('ref_axis',(1.,0.,0.));
#9535=DIRECTION('center_axis',(0.,-1.,0.));
#9536=DIRECTION('ref_axis',(1.,0.,0.));
#9537=DIRECTION('',(0.707106781186547,0.707106781186548,8.65956056235493E-17));
#9538=DIRECTION('center_axis',(0.,-1.,0.));
#9539=DIRECTION('ref_axis',(1.,0.,0.));
#9540=DIRECTION('center_axis',(0.,-1.,0.));
#9541=DIRECTION('ref_axis',(1.,0.,0.));
#9542=DIRECTION('',(0.,1.,0.));
#9543=DIRECTION('center_axis',(0.,1.,0.));
#9544=DIRECTION('ref_axis',(1.,0.,0.));
#9545=DIRECTION('center_axis',(0.,-1.,0.));
#9546=DIRECTION('ref_axis',(1.,0.,0.));
#9547=DIRECTION('',(-0.707106781186547,0.707106781186548,-8.65956056235493E-17));
#9548=DIRECTION('center_axis',(0.,-1.,0.));
#9549=DIRECTION('ref_axis',(0.,0.,-1.));
#9550=DIRECTION('center_axis',(0.,-1.,0.));
#9551=DIRECTION('ref_axis',(1.,0.,0.));
#9552=DIRECTION('center_axis',(0.,1.,0.));
#9553=DIRECTION('ref_axis',(1.,0.,0.));
#9554=DIRECTION('center_axis',(0.,1.,0.));
#9555=DIRECTION('ref_axis',(1.,0.,0.));
#9556=DIRECTION('',(-0.447213595499958,0.894427190999916,-5.47678698264203E-17));
#9557=DIRECTION('center_axis',(0.,-1.,0.));
#9558=DIRECTION('ref_axis',(1.,0.,0.));
#9559=DIRECTION('',(0.,1.,0.));
#11844=CARTESIAN_POINT('',(0.,0.,0.));
#11845=CARTESIAN_POINT('Origin',(0.0866025403784439,-0.4,-0.15));
#11846=CARTESIAN_POINT('',(0.173205080756888,-0.4,0.));
#11847=CARTESIAN_POINT('',(0.0866025403784439,-0.4,-0.15));
#11848=CARTESIAN_POINT('',(0.173205080756888,-0.4,0.));
#11849=CARTESIAN_POINT('',(0.0866025403784439,-0.64,-0.15));
#11850=CARTESIAN_POINT('',(0.0866025403784439,-0.4,-0.15));
#11851=CARTESIAN_POINT('',(0.173205080756888,-0.64,0.));
#11852=CARTESIAN_POINT('',(0.173205080756888,-0.64,0.));
#11853=CARTESIAN_POINT('',(0.173205080756888,-0.4,0.));
#11854=CARTESIAN_POINT('Origin',(-0.0866025403784438,-0.4,-0.15));
#11855=CARTESIAN_POINT('',(-0.0866025403784438,-0.4,-0.15));
#11856=CARTESIAN_POINT('',(0.0866025403784439,-0.4,-0.15));
#11857=CARTESIAN_POINT('',(-0.0866025403784438,-0.64,-0.15));
#11858=CARTESIAN_POINT('',(-0.0866025403784438,-0.4,-0.15));
#11859=CARTESIAN_POINT('',(0.0866025403784439,-0.64,-0.15));
#11860=CARTESIAN_POINT('Origin',(-0.173205080756888,-0.4,-2.77555756156289E-17));
#11861=CARTESIAN_POINT('',(-0.173205080756888,-0.4,-2.12115047744981E-17));
#11862=CARTESIAN_POINT('',(-0.0866025403784438,-0.4,-0.15));
#11863=CARTESIAN_POINT('',(-0.173205080756888,-0.64,-2.77555756156289E-17));
#11864=CARTESIAN_POINT('',(-0.173205080756888,-0.4,-2.12115047744981E-17));
#11865=CARTESIAN_POINT('',(-0.0866025403784438,-0.64,-0.15));
#11866=CARTESIAN_POINT('Origin',(-0.0866025403784439,-0.4,0.15));
#11867=CARTESIAN_POINT('',(-0.0866025403784439,-0.4,0.15));
#11868=CARTESIAN_POINT('',(-0.173205080756888,-0.4,-2.12115047744981E-17));
#11869=CARTESIAN_POINT('',(-0.0866025403784439,-0.64,0.15));
#11870=CARTESIAN_POINT('',(-0.0866025403784439,-0.4,0.15));
#11871=CARTESIAN_POINT('',(-0.173205080756888,-0.64,-2.12115047744981E-17));
#11872=CARTESIAN_POINT('Origin',(0.0866025403784439,-0.4,0.15));
#11873=CARTESIAN_POINT('',(0.0866025403784439,-0.4,0.15));
#11874=CARTESIAN_POINT('',(-0.0866025403784439,-0.4,0.15));
#11875=CARTESIAN_POINT('',(0.0866025403784439,-0.64,0.15));
#11876=CARTESIAN_POINT('',(0.0866025403784439,-0.4,0.15));
#11877=CARTESIAN_POINT('',(-0.0866025403784439,-0.64,0.15));
#11878=CARTESIAN_POINT('Origin',(0.173205080756888,-0.4,0.));
#11879=CARTESIAN_POINT('',(0.0866025403784439,-0.4,0.15));
#11880=CARTESIAN_POINT('',(0.0866025403784439,-0.64,0.15));
#11881=CARTESIAN_POINT('Origin',(0.,-0.4,-2.77555756156289E-17));
#11882=CARTESIAN_POINT('Origin',(0.,-0.64,-2.77555756156289E-17));
#11883=CARTESIAN_POINT('Origin',(0.,-1.,0.));
#11884=CARTESIAN_POINT('',(-0.1954,-1.,2.39295984553393E-17));
#11885=CARTESIAN_POINT('Origin',(0.,-1.,0.));
#11886=CARTESIAN_POINT('Origin',(0.3,0.4,0.));
#11887=CARTESIAN_POINT('',(-0.3,0.4,-3.67394039744206E-17));
#11888=CARTESIAN_POINT('Origin',(0.,0.4,0.));
#11889=CARTESIAN_POINT('Origin',(0.,0.375,0.));
#11890=CARTESIAN_POINT('',(-0.35,0.35,-4.28626379701573E-17));
#11891=CARTESIAN_POINT('Origin',(0.,0.35,0.));
#11892=CARTESIAN_POINT('',(-0.325,0.375,-3.9801020972289E-17));
#11893=CARTESIAN_POINT('Origin',(0.,0.19,0.));
#11894=CARTESIAN_POINT('',(-0.35,0.03,-4.28626379701574E-17));
#11895=CARTESIAN_POINT('Origin',(0.,0.03,0.));
#11896=CARTESIAN_POINT('',(-0.35,0.19,-4.28626379701574E-17));
#11897=CARTESIAN_POINT('Origin',(0.,0.0149999999999999,0.));
#11898=CARTESIAN_POINT('',(-0.32,-3.29597460435593E-17,-3.91886975727153E-17));
#11899=CARTESIAN_POINT('Origin',(0.,0.,0.));
#11900=CARTESIAN_POINT('',(-0.335,0.0149999999999999,-4.10256677714363E-17));
#11901=CARTESIAN_POINT('Origin',(0.22,0.,0.));
#11902=CARTESIAN_POINT('',(-0.22,-6.93889390390723E-18,-2.69422295812418E-17));
#11903=CARTESIAN_POINT('Origin',(0.,0.,0.));
#11904=CARTESIAN_POINT('Origin',(0.,-0.02,0.));
#11905=CARTESIAN_POINT('',(-0.1954,-0.0492,2.39295984553393E-17));
#11906=CARTESIAN_POINT('Origin',(0.,-0.0492,0.));
#11907=CARTESIAN_POINT('',(-0.21,-0.02,-2.57175827820944E-17));
#11908=CARTESIAN_POINT('Origin',(0.,-0.8,0.));
#11909=CARTESIAN_POINT('',(-0.1954,-0.8,-2.39295984553393E-17));
#12356=UNCERTAINTY_MEASURE_WITH_UNIT(LENGTH_MEASURE(0.001),#12414,
'DISTANCE_ACCURACY_VALUE',
'Maximum model space distance between geometric entities at asserted c
onnectivities');
#12367=UNCERTAINTY_MEASURE_WITH_UNIT(LENGTH_MEASURE(0.001),#12414,
'DISTANCE_ACCURACY_VALUE',
'Maximum model space distance between geometric entities at asserted c
onnectivities');
#12402=(
GEOMETRIC_REPRESENTATION_CONTEXT(3)
GLOBAL_UNCERTAINTY_ASSIGNED_CONTEXT((#12356))
GLOBAL_UNIT_ASSIGNED_CONTEXT((#12414,#12416,#12417))
REPRESENTATION_CONTEXT('','3D')
);
#12413=(
GEOMETRIC_REPRESENTATION_CONTEXT(3)
GLOBAL_UNCERTAINTY_ASSIGNED_CONTEXT((#12367))
GLOBAL_UNIT_ASSIGNED_CONTEXT((#12414,#12416,#12417))
REPRESENTATION_CONTEXT('','3D')
);
#12414=(
LENGTH_UNIT()
NAMED_UNIT(*)
SI_UNIT(.CENTI.,.METRE.)
);
#12416=(
NAMED_UNIT(*)
PLANE_ANGLE_UNIT()
SI_UNIT($,.RADIAN.)
);
#12417=(
NAMED_UNIT(*)
SI_UNIT($,.STERADIAN.)
SOLID_ANGLE_UNIT()
);
#12452=SHAPE_DEFINITION_REPRESENTATION(#12504,#12605);
#12504=PRODUCT_DEFINITION_SHAPE('',$,#12651);
#12605=SHAPE_REPRESENTATION('',(#7678),#12402);
#12616=PRODUCT_DEFINITION_CONTEXT('part definition',#12753,'design');
#12651=PRODUCT_DEFINITION('M4x10 Cap Screw','M4x10 Cap Screw',#12696,#12616);
#12696=PRODUCT_DEFINITION_FORMATION('',$,#12789);
#12753=APPLICATION_CONTEXT(
'Core Data for Automotive Mechanical Design Process');
#12754=PRODUCT_CONTEXT('part definition',#12753,'mechanical');
#12789=PRODUCT('M4x10 Cap Screw','M4x10 Cap Screw','M4x10 Cap Screw',(#12754));
#12870=COLOUR_RGB('Black',0.12,0.14,0.17);
#12871=FILL_AREA_STYLE_COLOUR('',#12870);
#12872=FILL_AREA_STYLE('',(#12871));
#12873=SURFACE_STYLE_FILL_AREA(#12872);
#12874=SURFACE_SIDE_STYLE('',(#12873));
#12875=SURFACE_STYLE_USAGE(.BOTH.,#12874);
#12876=PRESENTATION_STYLE_ASSIGNMENT((#12875));
ENDSEC;
END-ISO-10303-21;
